ISO-10303-21;
HEADER;
/* Generated by software containing ST-Developer
 * from STEP Tools, Inc. (www.steptools.com) 
 */

FILE_DESCRIPTION(
/* description */ ('Air blow-off nozzle station'),
/* implementation_level */ '2;1');

FILE_NAME(
/* name */ 'Ball clamp nut.step',
/* time_stamp */ '2026-10-27T10:53:54-07:00',
/* author */ (''),
/* organization */ (''),
/* preprocessor_version */ 'ST-DEVELOPER v20.2',
/* originating_system */ 'Autodesk Translation Framework v15.17.0.0',
/* authorisation */ '');

FILE_SCHEMA (('AUTOMOTIVE_DESIGN { 1 0 10303 214 3 1 1 }'));
ENDSEC;

DATA;
#10=MECHANICAL_DESIGN_GEOMETRIC_PRESENTATION_REPRESENTATION('',(#243),#7897);
#165=SPHERICAL_SURFACE('',#4702,1.);
#193=SHAPE_REPRESENTATION_RELATIONSHIP('SRR','None',#8007,#218);
#218=ADVANCED_BREP_SHAPE_REPRESENTATION('',(#268),#7874);
#243=STYLED_ITEM('',(#8227),#268);
#268=MANIFOLD_SOLID_BREP('Body1',#4292);
#310=FACE_BOUND('',#885,.T.);
#311=FACE_BOUND('',#886,.T.);
#312=FACE_BOUND('',#889,.T.);
#313=FACE_BOUND('',#892,.T.);
#314=FACE_BOUND('',#894,.T.);
#415=PLANE('',#4707);
#416=PLANE('',#4711);
#417=PLANE('',#4712);
#601=FACE_OUTER_BOUND('',#882,.T.);
#602=FACE_OUTER_BOUND('',#883,.T.);
#603=FACE_OUTER_BOUND('',#884,.T.);
#604=FACE_OUTER_BOUND('',#887,.T.);
#605=FACE_OUTER_BOUND('',#888,.T.);
#606=FACE_OUTER_BOUND('',#890,.T.);
#607=FACE_OUTER_BOUND('',#891,.T.);
#608=FACE_OUTER_BOUND('',#893,.T.);
#882=EDGE_LOOP('',(#3175,#3176,#3177,#3178));
#883=EDGE_LOOP('',(#3179,#3180,#3181,#3182));
#884=EDGE_LOOP('',(#3183,#3184));
#885=EDGE_LOOP('',(#3185));
#886=EDGE_LOOP('',(#3186));
#887=EDGE_LOOP('',(#3187,#3188,#3189,#3190));
#888=EDGE_LOOP('',(#3191));
#889=EDGE_LOOP('',(#3192));
#890=EDGE_LOOP('',(#3193,#3194,#3195,#3196));
#891=EDGE_LOOP('',(#3197));
#892=EDGE_LOOP('',(#3198));
#893=EDGE_LOOP('',(#3199));
#894=EDGE_LOOP('',(#3200));
#1224=LINE('',#6928,#1578);
#1225=LINE('',#6934,#1579);
#1226=LINE('',#6944,#1580);
#1227=LINE('',#6951,#1581);
#1578=VECTOR('',#5376,0.4);
#1579=VECTOR('',#5383,0.85);
#1580=VECTOR('',#5394,1.2);
#1581=VECTOR('',#5403,1.4);
#1883=CIRCLE('',#4697,0.4);
#1884=CIRCLE('',#4698,0.4);
#1885=CIRCLE('',#4700,0.85);
#1886=CIRCLE('',#4701,0.85);
#1887=CIRCLE('',#4703,1.);
#1888=CIRCLE('',#4705,1.2);
#1889=CIRCLE('',#4706,1.2);
#1890=CIRCLE('',#4709,1.4);
#1891=CIRCLE('',#4710,1.4);
#2100=VERTEX_POINT('',#6925);
#2101=VERTEX_POINT('',#6927);
#2102=VERTEX_POINT('',#6931);
#2103=VERTEX_POINT('',#6933);
#2104=VERTEX_POINT('',#6937);
#2105=VERTEX_POINT('',#6938);
#2106=VERTEX_POINT('',#6941);
#2107=VERTEX_POINT('',#6943);
#2108=VERTEX_POINT('',#6948);
#2109=VERTEX_POINT('',#6950);
#2505=EDGE_CURVE('',#2100,#2100,#1883,.T.);
#2506=EDGE_CURVE('',#2100,#2101,#1224,.T.);
#2507=EDGE_CURVE('',#2101,#2101,#1884,.T.);
#2508=EDGE_CURVE('',#2102,#2102,#1885,.T.);
#2509=EDGE_CURVE('',#2102,#2103,#1225,.T.);
#2510=EDGE_CURVE('',#2103,#2103,#1886,.T.);
#2511=EDGE_CURVE('',#2104,#2105,#1887,.T.);
#2512=EDGE_CURVE('',#2106,#2106,#1888,.T.);
#2513=EDGE_CURVE('',#2106,#2107,#1226,.T.);
#2514=EDGE_CURVE('',#2107,#2107,#1889,.T.);
#2515=EDGE_CURVE('',#2108,#2108,#1890,.T.);
#2516=EDGE_CURVE('',#2108,#2109,#1227,.T.);
#2517=EDGE_CURVE('',#2109,#2109,#1891,.T.);
#3175=ORIENTED_EDGE('',*,*,#2505,.F.);
#3176=ORIENTED_EDGE('',*,*,#2506,.T.);
#3177=ORIENTED_EDGE('',*,*,#2507,.F.);
#3178=ORIENTED_EDGE('',*,*,#2506,.F.);
#3179=ORIENTED_EDGE('',*,*,#2508,.F.);
#3180=ORIENTED_EDGE('',*,*,#2509,.T.);
#3181=ORIENTED_EDGE('',*,*,#2510,.F.);
#3182=ORIENTED_EDGE('',*,*,#2509,.F.);
#3183=ORIENTED_EDGE('',*,*,#2511,.T.);
#3184=ORIENTED_EDGE('',*,*,#2511,.F.);
#3185=ORIENTED_EDGE('',*,*,#2505,.T.);
#3186=ORIENTED_EDGE('',*,*,#2510,.T.);
#3187=ORIENTED_EDGE('',*,*,#2512,.F.);
#3188=ORIENTED_EDGE('',*,*,#2513,.T.);
#3189=ORIENTED_EDGE('',*,*,#2514,.F.);
#3190=ORIENTED_EDGE('',*,*,#2513,.F.);
#3191=ORIENTED_EDGE('',*,*,#2512,.T.);
#3192=ORIENTED_EDGE('',*,*,#2507,.T.);
#3193=ORIENTED_EDGE('',*,*,#2515,.F.);
#3194=ORIENTED_EDGE('',*,*,#2516,.T.);
#3195=ORIENTED_EDGE('',*,*,#2517,.T.);
#3196=ORIENTED_EDGE('',*,*,#2516,.F.);
#3197=ORIENTED_EDGE('',*,*,#2515,.T.);
#3198=ORIENTED_EDGE('',*,*,#2514,.T.);
#3199=ORIENTED_EDGE('',*,*,#2517,.F.);
#3200=ORIENTED_EDGE('',*,*,#2508,.T.);
#3976=CYLINDRICAL_SURFACE('',#4696,0.4);
#3977=CYLINDRICAL_SURFACE('',#4699,0.85);
#3978=CYLINDRICAL_SURFACE('',#4704,1.2);
#3979=CYLINDRICAL_SURFACE('',#4708,1.4);
#4091=ADVANCED_FACE('',(#601),#3976,.F.);
#4092=ADVANCED_FACE('',(#602),#3977,.F.);
#4093=ADVANCED_FACE('',(#603,#310,#311),#165,.F.);
#4094=ADVANCED_FACE('',(#604),#3978,.T.);
#4095=ADVANCED_FACE('',(#605,#312),#415,.T.);
#4096=ADVANCED_FACE('',(#606),#3979,.T.);
#4097=ADVANCED_FACE('',(#607,#313),#416,.T.);
#4098=ADVANCED_FACE('',(#608,#314),#417,.F.);
#4292=CLOSED_SHELL('',(#4091,#4092,#4093,#4094,#4095,#4096,#4097,#4098));
#4695=AXIS2_PLACEMENT_3D('',#6923,#5370,#5371);
#4696=AXIS2_PLACEMENT_3D('',#6924,#5372,#5373);
#4697=AXIS2_PLACEMENT_3D('',#6926,#5374,#5375);
#4698=AXIS2_PLACEMENT_3D('',#6929,#5377,#5378);
#4699=AXIS2_PLACEMENT_3D('',#6930,#5379,#5380);
#4700=AXIS2_PLACEMENT_3D('',#6932,#5381,#5382);
#4701=AXIS2_PLACEMENT_3D('',#6935,#5384,#5385);
#4702=AXIS2_PLACEMENT_3D('',#6936,#5386,#5387);
#4703=AXIS2_PLACEMENT_3D('',#6939,#5388,#5389);
#4704=AXIS2_PLACEMENT_3D('',#6940,#5390,#5391);
#4705=AXIS2_PLACEMENT_3D('',#6942,#5392,#5393);
#4706=AXIS2_PLACEMENT_3D('',#6945,#5395,#5396);
#4707=AXIS2_PLACEMENT_3D('',#6946,#5397,#5398);
#4708=AXIS2_PLACEMENT_3D('',#6947,#5399,#5400);
#4709=AXIS2_PLACEMENT_3D('',#6949,#5401,#5402);
#4710=AXIS2_PLACEMENT_3D('',#6952,#5404,#5405);
#4711=AXIS2_PLACEMENT_3D('',#6953,#5406,#5407);
#4712=AXIS2_PLACEMENT_3D('',#6954,#5408,#5409);
#5370=DIRECTION('axis',(0.,0.,1.));
#5371=DIRECTION('refdir',(1.,0.,0.));
#5372=DIRECTION('center_axis',(0.,1.,0.));
#5373=DIRECTION('ref_axis',(1.,0.,0.));
#5374=DIRECTION('center_axis',(0.,1.,0.));
#5375=DIRECTION('ref_axis',(1.,0.,0.));
#5376=DIRECTION('',(0.,1.,0.));
#5377=DIRECTION('center_axis',(0.,-1.,0.));
#5378=DIRECTION('ref_axis',(1.,0.,0.));
#5379=DIRECTION('center_axis',(0.,1.,0.));
#5380=DIRECTION('ref_axis',(1.,0.,0.));
#5381=DIRECTION('center_axis',(0.,1.,0.));
#5382=DIRECTION('ref_axis',(1.,0.,0.));
#5383=DIRECTION('',(0.,1.,0.));
#5384=DIRECTION('center_axis',(0.,-1.,0.));
#5385=DIRECTION('ref_axis',(1.,0.,0.));
#5386=DIRECTION('center_axis',(0.,0.,1.));
#5387=DIRECTION('ref_axis',(1.,0.,0.));
#5388=DIRECTION('center_axis',(0.,1.,0.));
#5389=DIRECTION('ref_axis',(-1.,0.,0.));
#5390=DIRECTION('center_axis',(0.,1.,0.));
#5391=DIRECTION('ref_axis',(1.,0.,0.));
#5392=DIRECTION('center_axis',(0.,1.,0.));
#5393=DIRECTION('ref_axis',(1.,0.,0.));
#5394=DIRECTION('',(0.,-1.,0.));
#5395=DIRECTION('center_axis',(0.,-1.,0.));
#5396=DIRECTION('ref_axis',(1.,0.,0.));
#5397=DIRECTION('center_axis',(0.,1.,0.));
#5398=DIRECTION('ref_axis',(1.,0.,0.));
#5399=DIRECTION('center_axis',(0.,1.,0.));
#5400=DIRECTION('ref_axis',(1.,0.,0.));
#5401=DIRECTION('center_axis',(0.,1.,0.));
#5402=DIRECTION('ref_axis',(1.,0.,0.));
#5403=DIRECTION('',(0.,-1.,0.));
#5404=DIRECTION('center_axis',(0.,1.,0.));
#5405=DIRECTION('ref_axis',(1.,0.,0.));
#5406=DIRECTION('center_axis',(0.,1.,0.));
#5407=DIRECTION('ref_axis',(1.,0.,0.));
#5408=DIRECTION('center_axis',(0.,1.,0.));
#5409=DIRECTION('ref_axis',(1.,0.,0.));
#6923=CARTESIAN_POINT('',(0.,0.,0.));
#6924=CARTESIAN_POINT('Origin',(-3.,-2.1,23.));
#6925=CARTESIAN_POINT('',(-3.4,-1.08348486100883,23.));
#6926=CARTESIAN_POINT('Origin',(-3.,-1.08348486100883,23.));
#6927=CARTESIAN_POINT('',(-3.4,-1.,23.));
#6928=CARTESIAN_POINT('',(-3.4,-2.1,23.));
#6929=CARTESIAN_POINT('Origin',(-3.,-1.,23.));
#6930=CARTESIAN_POINT('Origin',(-3.,-3.3,23.));
#6931=CARTESIAN_POINT('',(-3.85,-3.2,23.));
#6932=CARTESIAN_POINT('Origin',(-3.,-3.2,23.));
#6933=CARTESIAN_POINT('',(-3.85,-2.52678268764264,23.));
#6934=CARTESIAN_POINT('',(-3.85,-3.3,23.));
#6935=CARTESIAN_POINT('Origin',(-3.,-2.52678268764264,23.));
#6936=CARTESIAN_POINT('Origin',(-3.,-2.,23.));
#6937=CARTESIAN_POINT('',(-3.,-2.,22.));
#6938=CARTESIAN_POINT('',(-3.,-2.,24.));
#6939=CARTESIAN_POINT('Origin',(-3.,-2.,23.));
#6940=CARTESIAN_POINT('Origin',(-3.,-1.5,23.));
#6941=CARTESIAN_POINT('',(-4.2,-1.,23.));
#6942=CARTESIAN_POINT('Origin',(-3.,-1.,23.));
#6943=CARTESIAN_POINT('',(-4.2,-1.5,23.));
#6944=CARTESIAN_POINT('',(-4.2,-1.5,23.));
#6945=CARTESIAN_POINT('Origin',(-3.,-1.5,23.));
#6946=CARTESIAN_POINT('Origin',(-3.,-1.,23.));
#6947=CARTESIAN_POINT('Origin',(-3.,-3.2,23.));
#6948=CARTESIAN_POINT('',(-4.4,-1.5,23.));
#6949=CARTESIAN_POINT('Origin',(-3.,-1.5,23.));
#6950=CARTESIAN_POINT('',(-4.4,-3.2,23.));
#6951=CARTESIAN_POINT('',(-4.4,-3.2,23.));
#6952=CARTESIAN_POINT('Origin',(-3.,-3.2,23.));
#6953=CARTESIAN_POINT('Origin',(-3.,-1.5,23.));
#6954=CARTESIAN_POINT('Origin',(-3.,-3.2,23.));
#7842=UNCERTAINTY_MEASURE_WITH_UNIT(LENGTH_MEASURE(0.001),#7898,
'DISTANCE_ACCURACY_VALUE',
'Maximum model space distance between geometric entities at asserted c
onnectivities');
#7865=UNCERTAINTY_MEASURE_WITH_UNIT(LENGTH_MEASURE(0.001),#7898,
'DISTANCE_ACCURACY_VALUE',
'Maximum model space distance between geometric entities at asserted c
onnectivities');
#7874=(
GEOMETRIC_REPRESENTATION_CONTEXT(3)
GLOBAL_UNCERTAINTY_ASSIGNED_CONTEXT((#7842))
GLOBAL_UNIT_ASSIGNED_CONTEXT((#7898,#7900,#7901))
REPRESENTATION_CONTEXT('','3D')
);
#7897=(
GEOMETRIC_REPRESENTATION_CONTEXT(3)
GLOBAL_UNCERTAINTY_ASSIGNED_CONTEXT((#7865))
GLOBAL_UNIT_ASSIGNED_CONTEXT((#7898,#7900,#7901))
REPRESENTATION_CONTEXT('','3D')
);
#7898=(
LENGTH_UNIT()
NAMED_UNIT(*)
SI_UNIT(.CENTI.,.METRE.)
);
#7900=(
NAMED_UNIT(*)
PLANE_ANGLE_UNIT()
SI_UNIT($,.RADIAN.)
);
#7901=(
NAMED_UNIT(*)
SI_UNIT($,.STERADIAN.)
SOLID_ANGLE_UNIT()
);
#7910=SHAPE_DEFINITION_REPRESENTATION(#7941,#8007);
#7941=PRODUCT_DEFINITION_SHAPE('',$,#8039);
#8007=SHAPE_REPRESENTATION('',(#4695),#7874);
#8030=PRODUCT_DEFINITION_CONTEXT('part definition',#8125,'design');
#8039=PRODUCT_DEFINITION('Ball clamp nut','Ball clamp nut',#8070,#8030);
#8070=PRODUCT_DEFINITION_FORMATION('',$,#8135);
#8125=APPLICATION_CONTEXT(
'Core Data for Automotive Mechanical Design Process');
#8126=PRODUCT_CONTEXT('part definition',#8125,'mechanical');
#8135=PRODUCT('Ball clamp nut','Ball clamp nut','Ball clamp nut',(#8126));
#8221=COLOUR_RGB('Black',0.12,0.14,0.17);
#8222=FILL_AREA_STYLE_COLOUR('',#8221);
#8223=FILL_AREA_STYLE('',(#8222));
#8224=SURFACE_STYLE_FILL_AREA(#8223);
#8225=SURFACE_SIDE_STYLE('',(#8224));
#8226=SURFACE_STYLE_USAGE(.BOTH.,#8225);
#8227=PRESENTATION_STYLE_ASSIGNMENT((#8226));
ENDSEC;
END-ISO-10303-21;
